ISO-10303-21;
HEADER;
FILE_DESCRIPTION (('STEP AP203'),
    '1' );
FILE_NAME ('Pin 3.step',
    '2026-10-31T14:11:27',
    ( '' ),
    ( '' ),
    'SwSTEP 2.0',
    'SolidWorks 2024',
    '' );
FILE_SCHEMA (( 'AUTOMOTIVE_DESIGN' ));
ENDSEC;

DATA;
#29=CYLINDRICAL_SURFACE ( 'NONE', #10267, 4.750000000000001776 ) ;
#71=ORIENTED_EDGE ( 'NONE', *, *, #21028, .T. ) ;
#91=DIRECTION ( 'NONE',  ( 6.123230174520380038E-17, 4.962644601432250805E-15, 1.000000000000000000 ) ) ;
#128=AXIS2_PLACEMENT_3D ( 'NONE', #20499, #7802, #13149 ) ;
#139=CARTESIAN_POINT ( 'NONE',  ( 34.40556712239440174, 8.514986143070938596, -28.47000000000049980 ) ) ;
#153=CARTESIAN_POINT ( 'NONE',  ( 35.09747506357100377, 11.43410645592840069, -27.69000000000049866 ) ) ;
#276=DIRECTION ( 'NONE',  ( 6.123230174520380038E-17, 4.962644601432250805E-15, 1.000000000000000000 ) ) ;
#329=CARTESIAN_POINT ( 'NONE',  ( 37.27955344062029752, 9.375336445360510140, -29.25000000000050093 ) ) ;
#331=CARTESIAN_POINT ( 'NONE',  ( 35.24824457160689661, 8.315249525024576371, -27.55602540378494325 ) ) ;
#366=ORIENTED_EDGE ( 'NONE', *, *, #16049, .T. ) ;
#415=DIRECTION ( 'NONE',  ( 1.000000000000000000, 0.000000000000000000, 0.000000000000000000 ) ) ;
#454=ORIENTED_EDGE ( 'NONE', *, *, #21393, .F. ) ;
#458=CARTESIAN_POINT ( 'NONE',  ( 37.91003399039541222, 9.225896048119837545, -26.88000000000049639 ) ) ;
#506=CARTESIAN_POINT ( 'NONE',  ( 36.09092202081949807, 8.115512906978191054, -29.25000000000050093 ) ) ;
#524=DIRECTION ( 'NONE',  ( -0.9730401042858035643, 0.2306359803922031215, 0.000000000000000000 ) ) ;
#672=ORIENTED_EDGE ( 'NONE', *, *, #10946, .T. ) ;
#718=DIRECTION ( 'NONE',  ( 6.281952996264450405E-17, 4.969341027148649850E-15, 1.000000000000000000 ) ) ;
#763=DIRECTION ( 'NONE',  ( 0.1997366180463774621, 0.8426774492125632676, -0.5000000000000035527 ) ) ;
#866=VECTOR ( 'NONE', #10324, 1000.000000000000000 ) ;
#965=VERTEX_POINT ( 'NONE', #17524 ) ;
#1001=ADVANCED_FACE ( 'NONE', ( #1708 ), #29, .T. ) ;
#1036=CARTESIAN_POINT ( 'NONE',  ( 35.07420204808332898, 7.580974001528502093, -10.74538000000048932 ) ) ;
#1037=CARTESIAN_POINT ( 'NONE',  ( 37.27955344062029752, 9.375336445360519022, -27.69000000000049866 ) ) ;
#1039=ORIENTED_EDGE ( 'NONE', *, *, #16207, .T. ) ;
#1060=CARTESIAN_POINT ( 'NONE',  ( 36.09092202081949807, 8.115512906978191054, -28.47000000000049980 ) ) ;
#1062=VECTOR ( 'NONE', #21138, 1000.000000000000000 ) ;
#1082=ADVANCED_FACE ( 'NONE', ( #15852 ), #3259, .F. ) ;
#1088=ADVANCED_FACE ( 'NONE', ( #16198 ), #12427, .F. ) ;
#1091=CIRCLE ( 'NONE', #7186, 4.750000000000001776 ) ;
#1249=CIRCLE ( 'NONE', #8089, 4.750000000000001776 ) ;
#1270=CIRCLE ( 'NONE', #16075, 2.500000000000000444 ) ;
#1281=VERTEX_POINT ( 'NONE', #153 ) ;
#1372=ORIENTED_EDGE ( 'NONE', *, *, #5950, .F. ) ;
#1421=VECTOR ( 'NONE', #17606, 1000.000000000000000 ) ;
#1450=CARTESIAN_POINT ( 'NONE',  ( 34.50315935367051878, 10.80419468673720296, -27.44000000000050576 ) ) ;
#1458=ORIENTED_EDGE ( 'NONE', *, *, #5679, .F. ) ;
#1466=DIRECTION ( 'NONE',  ( 0.2306359803922040652, 0.9730401042858032312, -4.849856555169149244E-15 ) ) ;
#1471=CARTESIAN_POINT ( 'NONE',  ( 34.40556712239440174, 8.514986143070949254, -27.69000000000049866 ) ) ;
#1476=DIRECTION ( 'NONE',  ( -0.9730401042858046745, 0.2306359803921981810, 0.000000000000000000 ) ) ;
#1493=PRODUCT_DEFINITION_SHAPE ( 'NONE', 'NONE',  #14615 ) ;
#1572=FACE_OUTER_BOUND ( 'NONE', #16686, .T. ) ;
#1575=FACE_BOUND ( 'NONE', #10925, .T. ) ;
#1644=VERTEX_POINT ( 'NONE', #8942 ) ;
#1645=DIRECTION ( 'NONE',  ( -0.2306359803922019835, -0.9730401042858037863, 4.857225732735059075E-15 ) ) ;
#1695=CARTESIAN_POINT ( 'NONE',  ( 36.43025397111700414, 13.30208005948929895, -26.50000000000049738 ) ) ;
#1708=FACE_OUTER_BOUND ( 'NONE', #20836, .T. ) ;
#1737=VECTOR ( 'NONE', #16486, 1000.000000000000227 ) ;
#1761=VECTOR ( 'NONE', #2272, 1000.000000000000114 ) ;
#1785=CIRCLE ( 'NONE', #13936, 4.750000000000001776 ) ;
#1805=CARTESIAN_POINT ( 'NONE',  ( 35.59419854219520118, 9.774809681453358934, -10.50000000000050093 ) ) ;
#1826=CARTESIAN_POINT ( 'NONE',  ( 35.94015251278350576, 11.23436983788199761, -27.55602540378494325 ) ) ;
#1835=CARTESIAN_POINT ( 'NONE',  ( 35.59419854219520118, 9.774809681453278998, -26.88000000000049994 ) ) ;
#1918=CARTESIAN_POINT ( 'NONE',  ( 36.09092202081949807, 8.115512906978191054, -27.69000000000049866 ) ) ;
#1932=ADVANCED_FACE ( 'NONE', ( #9878 ), #11569, .T. ) ;
#1934=VERTEX_POINT ( 'NONE', #20554 ) ;
#1955=ORIENTED_EDGE ( 'NONE', *, *, #13990, .T. ) ;
#1959=DIRECTION ( 'NONE',  ( -6.281952996264290168E-17, -4.969341027148640384E-15, -1.000000000000000000 ) ) ;
#1994=ORIENTED_EDGE ( 'NONE', *, *, #6302, .F. ) ;
#2061=ORIENTED_EDGE ( 'NONE', *, *, #14467, .F. ) ;
#2074=DIRECTION ( 'NONE',  ( -6.123230174520380038E-17, -4.962644601432250805E-15, -1.000000000000000000 ) ) ;
#2094=CARTESIAN_POINT ( 'NONE',  ( 35.59419854219520118, 9.774809681453278998, -26.88000000000049994 ) ) ;
#2143=DIRECTION ( 'NONE',  ( 6.123230174520409620E-17, 4.962644601432260272E-15, 1.000000000000000000 ) ) ;
#2225=ORIENTED_EDGE ( 'NONE', *, *, #2852, .F. ) ;
#2236=EDGE_CURVE ( 'NONE', #2850, #22077, #5561, .T. ) ;
#2240=EDGE_LOOP ( 'NONE', ( #2333, #12408, #10818, #1955, #22375, #366 ) ) ;
#2257=CARTESIAN_POINT ( 'NONE',  ( 36.68971944905815974, 14.39675017681084945, -27.87500000000052580 ) ) ;
#2272=DIRECTION ( 'NONE',  ( 0.2867834340965239592, -0.9579954394086668268, 4.742590440343770138E-15 ) ) ;
#2297=( BOUNDED_CURVE ( )  B_SPLINE_CURVE ( 2, ( #19632, #16412, #1918 ),
 .UNSPECIFIED., .F., .F. ) 
 B_SPLINE_CURVE_WITH_KNOTS ( ( 3, 3 ),
 ( 0.000000000000000000, 0.1752654207116860208 ),
 .UNSPECIFIED. ) 
 CURVE ( )  GEOMETRIC_REPRESENTATION_ITEM ( )  RATIONAL_B_SPLINE_CURVE ( ( 1.000000000000000000, 1.154700538379239916, 1.000000000000000000 ) ) 
 REPRESENTATION_ITEM ( '' )  );
#2327=EDGE_CURVE ( 'NONE', #7180, #2526, #16151, .T. ) ;
#2332=CARTESIAN_POINT ( 'NONE',  ( 35.88249351768550355, 10.99110981181060076, -10.50000000000050093 ) ) ;
#2333=ORIENTED_EDGE ( 'NONE', *, *, #15603, .F. ) ;
#2357=CIRCLE ( 'NONE', #2741, 2.009239999999998805 ) ;
#2425=EDGE_CURVE ( 'NONE', #10416, #1644, #2500, .T. ) ;
#2457=CARTESIAN_POINT ( 'NONE',  ( 38.22140682376687693, 9.152092534394331125, -26.50000000000049383 ) ) ;
#2500=CIRCLE ( 'NONE', #16901, 2.500000000000000444 ) ;
#2526=VERTEX_POINT ( 'NONE', #16661 ) ;
#2527=CARTESIAN_POINT ( 'NONE',  ( 34.40556712239440174, 8.514986143070938596, -29.25000000000050093 ) ) ;
#2569=CARTESIAN_POINT ( 'NONE',  ( 0.000000000000000000, 0.000000000000000000, 0.000000000000000000 ) ) ;
#2603=EDGE_CURVE ( 'NONE', #22277, #21097, #4428, .T. ) ;
#2613=DIRECTION ( 'NONE',  ( -6.123230174520380038E-17, -4.962644601432250805E-15, -1.000000000000000000 ) ) ;
#2737=EDGE_LOOP ( 'NONE', ( #13650, #12915, #20633, #15109 ) ) ;
#2741=AXIS2_PLACEMENT_3D ( 'NONE', #1805, #17988, #8845 ) ;
#2850=VERTEX_POINT ( 'NONE', #21761 ) ;
#2852=EDGE_CURVE ( 'NONE', #3011, #7550, #2297, .T. ) ;
#2867=ORIENTED_EDGE ( 'NONE', *, *, #8427, .F. ) ;
#2884=VERTEX_POINT ( 'NONE', #14281 ) ;
#3011=VERTEX_POINT ( 'NONE', #1037 ) ;
#3033=( GEOMETRIC_REPRESENTATION_CONTEXT ( 3 ) GLOBAL_UNCERTAINTY_ASSIGNED_CONTEXT ( ( #3484 ) ) GLOBAL_UNIT_ASSIGNED_CONTEXT ( ( #6065, #16141, #14246 ) ) REPRESENTATION_CONTEXT ( 'NONE', 'WORKASPACE' ) );
#3090=SHAPE_REPRESENTATION_RELATIONSHIP ( 'NONE' , 'NONE' ,  #8415, #22945 ) ;
#3143=VERTEX_POINT ( 'NONE', #21227 ) ;
#3167=CARTESIAN_POINT ( 'NONE',  ( 32.96699026062352544, 10.39752682851222865, -26.30000000000050520 ) ) ;
#3202=CARTESIAN_POINT ( 'NONE',  ( 37.91003399039541222, 9.225896048119828663, -29.25000000000049738 ) ) ;
#3223=ORIENTED_EDGE ( 'NONE', *, *, #5299, .T. ) ;
#3229=CARTESIAN_POINT ( 'NONE',  ( 35.59419854219520118, 9.774809681453270116, -29.25000000000050093 ) ) ;
#3259=PLANE ( 'NONE',  #8723 ) ;
#3276=ORIENTED_EDGE ( 'NONE', *, *, #23444, .F. ) ;
#3333=AXIS2_PLACEMENT_3D ( 'NONE', #5989, #20601, #4443 ) ;
#3360=CARTESIAN_POINT ( 'NONE',  ( 35.94015251278350576, 11.23436983788199761, -27.55602540378494325 ) ) ;
#3447=ADVANCED_FACE ( 'NONE', ( #11390 ), #15155, .T. ) ;
#3484=UNCERTAINTY_MEASURE_WITH_UNIT (LENGTH_MEASURE( 1.000000000000000082E-05 ), #6065, 'distance_accuracy_value', 'NONE');
#3488=DIRECTION ( 'NONE',  ( -0.6862566701892794940, -0.7273594590164634832, 3.657607522630173034E-15 ) ) ;
#3495=AXIS2_PLACEMENT_3D ( 'NONE', #10628, #14399, #5501 ) ;
#3496=CARTESIAN_POINT ( 'NONE',  ( 33.27836309399498305, 10.32372331478670979, -29.25000000000050449 ) ) ;
#3551=LINE ( 'NONE', #14119, #3553 ) ;
#3553=VECTOR ( 'NONE', #10813, 1000.000000000000114 ) ;
#3634=CARTESIAN_POINT ( 'NONE',  ( 36.78282996199610722, 11.03463321983559986, -28.47000000000049980 ) ) ;
#3712=PLANE ( 'NONE',  #22067 ) ;
#3775=CIRCLE ( 'NONE', #21645, 0.2000000000000012046 ) ;
#3788=ORIENTED_EDGE ( 'NONE', *, *, #12033, .F. ) ;
#3835=ORIENTED_EDGE ( 'NONE', *, *, #23276, .F. ) ;
#3862=VERTEX_POINT ( 'NONE', #3976 ) ;
#3871=CARTESIAN_POINT ( 'NONE',  ( 35.09747506357100377, 11.43410645592840069, -28.47000000000049980 ) ) ;
#3899=ORIENTED_EDGE ( 'NONE', *, *, #8544, .F. ) ;
#3922=AXIS2_PLACEMENT_3D ( 'NONE', #21270, #19271, #8469 ) ;
#3927=ORIENTED_EDGE ( 'NONE', *, *, #8427, .T. ) ;
#3976=CARTESIAN_POINT ( 'NONE',  ( 36.78282996199610722, 11.03463321983559986, -27.69000000000049866 ) ) ;
#4036=ORIENTED_EDGE ( 'NONE', *, *, #21028, .F. ) ;
#4134=DIRECTION ( 'NONE',  ( 0.9730401042858046745, -0.2306359803921981810, 0.000000000000000000 ) ) ;
#4230=DIRECTION ( 'NONE',  ( 1.000000000000000000, -6.281952996264290168E-17, 3.503246160812045303E-47 ) ) ;
#4274=LINE ( 'NONE', #18780, #22419 ) ;
#4281=ORIENTED_EDGE ( 'NONE', *, *, #5923, .T. ) ;
#4357=ADVANCED_FACE ( 'NONE', ( #18205, #1575 ), #3712, .T. ) ;
#4381=CARTESIAN_POINT ( 'NONE',  ( 35.59419854219520118, 9.774809681453330512, -17.70000000000050022 ) ) ;
#4428=CIRCLE ( 'NONE', #12771, 2.369999999999999218 ) ;
#4443=DIRECTION ( 'NONE',  ( -0.2306359803922033713, -0.9730401042858033422, 5.180237729619581644E-15 ) ) ;
#4473=DIRECTION ( 'NONE',  ( -0.2306359803922041485, -0.9730401042858032312, 4.373252460445728664E-15 ) ) ;
#4513=DIRECTION ( 'NONE',  ( -6.123230174520380038E-17, -4.962644601432260272E-15, -1.000000000000000000 ) ) ;
#4525=VECTOR ( 'NONE', #12651, 1000.000000000000000 ) ;
#4636=ORIENTED_EDGE ( 'NONE', *, *, #6302, .T. ) ;
#4647=LINE ( 'NONE', #1060, #1062 ) ;
#4653=CARTESIAN_POINT ( 'NONE',  ( 35.59419854219520118, 9.774809681453278998, -26.50000000000049738 ) ) ;
#4681=VECTOR ( 'NONE', #17488, 1000.000000000000114 ) ;
#4690=CARTESIAN_POINT ( 'NONE',  ( 37.27955344062029752, 9.375336445360510140, -29.25000000000050093 ) ) ;
#4693=ORIENTED_EDGE ( 'NONE', *, *, #13482, .T. ) ;
#4720=ORIENTED_EDGE ( 'NONE', *, *, #10277, .T. ) ;
#4948=ORIENTED_EDGE ( 'NONE', *, *, #5679, .T. ) ;
#4962=CARTESIAN_POINT ( 'NONE',  ( 36.17078849317570644, 12.20740994216783726, -17.70000000000051088 ) ) ;
#4972=AXIS2_PLACEMENT_3D ( 'NONE', #9727, #8284, #6021 ) ;
#5049=AXIS2_PLACEMENT_3D ( 'NONE', #458, #11200, #7840 ) ;
#5092=LINE ( 'NONE', #4962, #16485 ) ;
#5157=DIRECTION ( 'NONE',  ( 0.9730401042858035643, -0.2306359803922029272, 1.531342102931249911E-15 ) ) ;
#5211=VERTEX_POINT ( 'NONE', #3202 ) ;
#5218=AXIS2_PLACEMENT_3D ( 'NONE', #18219, #18351, #15001 ) ;
#5227=ORIENTED_EDGE ( 'NONE', *, *, #16658, .T. ) ;
#5259=DIRECTION ( 'NONE',  ( 1.000000000000000000, -6.281952996264290168E-17, 3.503246160812045303E-47 ) ) ;
#5262=CLOSED_SHELL ( 'NONE', ( #6568, #1932, #19282, #11447, #3447, #1088, #19566, #23104, #4357, #19148, #11998, #21855, #8561, #1001, #15798, #16064, #1082, #15892, #6164, #6863, #7247 ) ) ;
#5271=CIRCLE ( 'NONE', #19687, 2.500000000000000444 ) ;
#5299=EDGE_CURVE ( 'NONE', #3862, #2850, #11255, .T. ) ;
#5377=DIRECTION ( 'NONE',  ( 0.1630842657209339019, 0.6880432561069519393, -0.7071067811865526798 ) ) ;
#5389=DIRECTION ( 'NONE',  ( -2.102818713247520211E-14, -6.140746379865968924E-31, -1.000000000000000000 ) ) ;
#5410=CIRCLE ( 'NONE', #17541, 2.699999999999998845 ) ;
#5501=DIRECTION ( 'NONE',  ( -4.625706045737360025E-15, 0.000000000000000000, 1.000000000000000000 ) ) ;
#5506=DIRECTION ( 'NONE',  ( -0.2306359803922040930, -0.9730401042858032312, 4.616450158279817280E-15 ) ) ;
#5549=VECTOR ( 'NONE', #2143, 1000.000000000000000 ) ;
#5555=EDGE_CURVE ( 'NONE', #20782, #10416, #5271, .T. ) ;
#5561=LINE ( 'NONE', #16370, #1737 ) ;
#5574=CARTESIAN_POINT ( 'NONE',  ( 35.59419854219520118, 9.774809681453358934, -10.74538000000049998 ) ) ;
#5627=( BOUNDED_CURVE ( )  B_SPLINE_CURVE ( 2, ( #18447, #20680, #18683 ),
 .UNSPECIFIED., .F., .F. ) 
 B_SPLINE_CURVE_WITH_KNOTS ( ( 3, 3 ),
 ( 0.000000000000000000, 0.08763271035584535573 ),
 .UNSPECIFIED. ) 
 CURVE ( )  GEOMETRIC_REPRESENTATION_ITEM ( )  RATIONAL_B_SPLINE_CURVE ( ( 1.000000000000000000, 1.077350269189627063, 1.077350269189624843 ) ) 
 REPRESENTATION_ITEM ( '' )  );
#5679=EDGE_CURVE ( 'NONE', #21097, #11071, #1091, .T. ) ;
#5715=CARTESIAN_POINT ( 'NONE',  ( 36.05760157943842614, 11.72988078058856942, -10.50000000000050981 ) ) ;
#5848=EDGE_LOOP ( 'NONE', ( #1994, #22174 ) ) ;
#5916=ORIENTED_EDGE ( 'NONE', *, *, #14511, .T. ) ;
#5923=EDGE_CURVE ( 'NONE', #20782, #12824, #10989, .T. ) ;
#5950=EDGE_CURVE ( 'NONE', #22077, #1934, #7296, .T. ) ;
#5970=PLANE ( 'NONE',  #16723 ) ;
#5989=CARTESIAN_POINT ( 'NONE',  ( 35.59419854219520118, 9.774809681453358934, -10.50000000000050093 ) ) ;
#6021=DIRECTION ( 'NONE',  ( 0.2306359803922022056, 0.9730401042858037863, -4.163336342344340971E-15 ) ) ;
#6061=CARTESIAN_POINT ( 'NONE',  ( 37.03119170130820237, 10.20498483259809497, -27.44000000000050576 ) ) ;
#6065=( LENGTH_UNIT ( ) NAMED_UNIT ( * ) SI_UNIT ( .MILLI., .METRE. ) );
#6130=DIRECTION ( 'NONE',  ( 6.281952996264450405E-17, 4.969341027148649850E-15, 1.000000000000000000 ) ) ;
#6164=ADVANCED_FACE ( 'NONE', ( #16775 ), #5970, .F. ) ;
#6262=ORIENTED_EDGE ( 'NONE', *, *, #13132, .F. ) ;
#6302=EDGE_CURVE ( 'NONE', #5211, #22277, #20246, .T. ) ;
#6458=PLANE ( 'NONE',  #3495 ) ;
#6568=ADVANCED_FACE ( 'NONE', ( #16616 ), #17154, .F. ) ;
#6593=CIRCLE ( 'NONE', #15690, 4.750000000000001776 ) ;
#6617=DIRECTION ( 'NONE',  ( 0.2306359803922020946, 0.9730401042858036753, -4.006172263299086280E-15 ) ) ;
#6669=EDGE_CURVE ( 'NONE', #3862, #3011, #9744, .T. ) ;
#6863=ADVANCED_FACE ( 'NONE', ( #16137 ), #14476, .F. ) ;
#6992=AXIS2_PLACEMENT_3D ( 'NONE', #22557, #4513, #16739 ) ;
#7027=EDGE_CURVE ( 'NONE', #12824, #15703, #19083, .T. ) ;
#7053=VECTOR ( 'NONE', #763, 999.9999999999998863 ) ;
#7055=EDGE_CURVE ( 'NONE', #16863, #22020, #20969, .T. ) ;
#7063=DIRECTION ( 'NONE',  ( 0.9579954394086668268, 0.2867834340965239592, -1.485305508172449974E-15 ) ) ;
#7109=VECTOR ( 'NONE', #16523, 1000.000000000000000 ) ;
#7150=ORIENTED_EDGE ( 'NONE', *, *, #20881, .F. ) ;
#7167=CARTESIAN_POINT ( 'NONE',  ( 35.01760859121470304, 7.342209420738848635, -10.99076000000048836 ) ) ;
#7180=VERTEX_POINT ( 'NONE', #14074 ) ;
#7181=CARTESIAN_POINT ( 'NONE',  ( 35.01760859121468172, 7.342209420738772252, -26.30000000000049099 ) ) ;
#7186=AXIS2_PLACEMENT_3D ( 'NONE', #19529, #8851, #17403 ) ;
#7247=ADVANCED_FACE ( 'NONE', ( #10426 ), #11919, .F. ) ;
#7296=LINE ( 'NONE', #16533, #17815 ) ;
#7544=CARTESIAN_POINT ( 'NONE',  ( 35.59419854219520118, 9.774809681453278998, -26.30000000000050164 ) ) ;
#7550=VERTEX_POINT ( 'NONE', #16789 ) ;
#7562=LINE ( 'NONE', #9340, #7053 ) ;
#7595=VECTOR ( 'NONE', #1959, 1000.000000000000000 ) ;
#7678=FACE_OUTER_BOUND ( 'NONE', #11229, .T. ) ;
#7690=CARTESIAN_POINT ( 'NONE',  ( 36.17078849317571354, 12.20740994216786746, -10.99076000000051145 ) ) ;
#7760=DIRECTION ( 'NONE',  ( -0.9730401042858034533, 0.2306359803922031215, 0.000000000000000000 ) ) ;
#7763=DIRECTION ( 'NONE',  ( 0.6862566701892789389, 0.7273594590164639273, -3.657607522630180133E-15 ) ) ;
#7777=EDGE_CURVE ( 'NONE', #11668, #12386, #16108, .T. ) ;
#7791=EDGE_LOOP ( 'NONE', ( #18057, #4281, #11232, #3835, #18872 ) ) ;
#7802=DIRECTION ( 'NONE',  ( -6.281952996264290168E-17, -4.969341027148640384E-15, -1.000000000000000000 ) ) ;
#7840=DIRECTION ( 'NONE',  ( 0.9730401042858035643, -0.2306359803922027607, 0.000000000000000000 ) ) ;
#7851=VECTOR ( 'NONE', #9338, 1000.000000000000000 ) ;
#7892=CARTESIAN_POINT ( 'NONE',  ( 34.40556712239440174, 8.514986143070949254, -27.69000000000049866 ) ) ;
#7918=CIRCLE ( 'NONE', #11320, 2.380000000000002114 ) ;
#8036=DIRECTION ( 'NONE',  ( 3.121716675495546285E-31, 4.969341027148640384E-15, 1.000000000000000000 ) ) ;
#8075=DIRECTION ( 'NONE',  ( -0.1630842657209340962, -0.6880432561069589337, -0.7071067811865457964 ) ) ;
#8089=AXIS2_PLACEMENT_3D ( 'NONE', #23012, #2613, #17579 ) ;
#8091=AXIS2_PLACEMENT_3D ( 'NONE', #14406, #8959, #5506 ) ;
#8096=CARTESIAN_POINT ( 'NONE',  ( 37.27955344062029752, 9.375336445360519022, -27.69000000000049866 ) ) ;
#8110=DIRECTION ( 'NONE',  ( 0.2306359803922025109, 0.9730401042858035643, -5.112869192352692394E-15 ) ) ;
#8116=ORIENTED_EDGE ( 'NONE', *, *, #2603, .T. ) ;
#8284=DIRECTION ( 'NONE',  ( 6.123230174520370177E-17, 4.962644601432260272E-15, 1.000000000000000000 ) ) ;
#8385=CARTESIAN_POINT ( 'NONE',  ( 35.59419854219520118, 9.774809681453278998, -27.19000000000049866 ) ) ;
#8415=SHAPE_REPRESENTATION ( 'Pin 3', ( #12739 ), #3033 ) ;
#8427=EDGE_CURVE ( 'NONE', #1644, #16863, #1270, .T. ) ;
#8456=DIRECTION ( 'NONE',  ( 6.123230174520380038E-17, 4.962644601432250805E-15, 1.000000000000000000 ) ) ;
#8469=DIRECTION ( 'NONE',  ( 0.9730401042858035643, -0.2306359803922029272, 1.531342102931249911E-15 ) ) ;
#8486=EDGE_CURVE ( 'NONE', #3143, #12984, #6593, .T. ) ;
#8533=ORIENTED_EDGE ( 'NONE', *, *, #16743, .T. ) ;
#8544=EDGE_CURVE ( 'NONE', #1934, #17514, #9465, .T. ) ;
#8561=ADVANCED_FACE ( 'NONE', ( #18145, #16347 ), #22386, .T. ) ;
#8624=AXIS2_PLACEMENT_3D ( 'NONE', #14194, #21431, #5157 ) ;
#8650=CONICAL_SURFACE ( 'NONE', #21901, 2.254620000000000068, 0.7853981633974461696 ) ;
#8713=CARTESIAN_POINT ( 'NONE',  ( 35.09747506357100377, 11.43410645592840069, -27.69000000000049866 ) ) ;
#8723=AXIS2_PLACEMENT_3D ( 'NONE', #10526, #1466, #5389 ) ;
#8844=LINE ( 'NONE', #139, #7109 ) ;
#8845=DIRECTION ( 'NONE',  ( -0.2306359803922033713, -0.9730401042858033422, 5.180237729619581644E-15 ) ) ;
#8851=DIRECTION ( 'NONE',  ( -6.123230174520380038E-17, -4.962644601432250805E-15, -1.000000000000000000 ) ) ;
#8859=CARTESIAN_POINT ( 'NONE',  ( 35.59419854219520118, 9.774809681453278998, -27.87500000000050093 ) ) ;
#8875=DIRECTION ( 'NONE',  ( 0.2306359803922025109, 0.9730401042858035643, -5.112869192352692394E-15 ) ) ;
#8881=ORIENTED_EDGE ( 'NONE', *, *, #16658, .F. ) ;
#8902=ORIENTED_EDGE ( 'NONE', *, *, #12310, .F. ) ;
#8925=CARTESIAN_POINT ( 'NONE',  ( 33.90884364377009774, 10.17428291754599989, -27.69000000000049866 ) ) ;
#8942=CARTESIAN_POINT ( 'NONE',  ( 36.17078849317569933, 12.20740994216779107, -26.30000000000050875 ) ) ;
#8959=DIRECTION ( 'NONE',  ( -6.193954341422139021E-17, -4.965628413872130537E-15, -1.000000000000000000 ) ) ;
#9042=ORIENTED_EDGE ( 'NONE', *, *, #6669, .T. ) ;
#9072=DIRECTION ( 'NONE',  ( 6.123230174520409620E-17, 4.962644601432260272E-15, 1.000000000000000000 ) ) ;
#9086=DIRECTION ( 'NONE',  ( -0.2306359803922019835, -0.9730401042858037863, 4.163336342344336238E-15 ) ) ;
#9130=ORIENTED_EDGE ( 'NONE', *, *, #7055, .T. ) ;
#9246=ORIENTED_EDGE ( 'NONE', *, *, #6669, .F. ) ;
#9258=DIRECTION ( 'NONE',  ( -0.9579954394086668268, -0.2867834340965239592, 1.485305508172449974E-15 ) ) ;
#9272=FACE_OUTER_BOUND ( 'NONE', #2737, .T. ) ;
#9307=CARTESIAN_POINT ( 'NONE',  ( 35.01760859121469593, 7.342209420738822878, -17.70000000000048956 ) ) ;
#9338=DIRECTION ( 'NONE',  ( -6.281952996264290168E-17, -4.969341027148640384E-15, -1.000000000000000000 ) ) ;
#9340=CARTESIAN_POINT ( 'NONE',  ( 35.79393516024157407, 10.61748713066584671, -27.19000000000050221 ) ) ;
#9465=LINE ( 'NONE', #23350, #19487 ) ;
#9468=DIRECTION ( 'NONE',  ( 6.281952996264339472E-17, 4.969341027148640384E-15, 1.000000000000000000 ) ) ;
#9568=DIRECTION ( 'NONE',  ( 0.2306359803922029827, 0.9730401042858035643, -4.849856555169150033E-15 ) ) ;
#9573=MANIFOLD_SOLID_BREP ( 'Imported1', #5262 ) ;
#9620=ORIENTED_EDGE ( 'NONE', *, *, #23276, .T. ) ;
#9669=CARTESIAN_POINT ( 'NONE',  ( 36.68971944905815974, 14.39675017681084768, -26.88000000000052481 ) ) ;
#9670=CARTESIAN_POINT ( 'NONE',  ( 35.59419854219520118, 9.774809681453278998, -26.50000000000049738 ) ) ;
#9679=DIRECTION ( 'NONE',  ( -0.2306359803922031215, -0.9730401042858034533, 4.849856555169147667E-15 ) ) ;
#9691=EDGE_CURVE ( 'NONE', #7550, #11668, #5627, .T. ) ;
#9717=CARTESIAN_POINT ( 'NONE',  ( 35.59419854219520118, 9.774809681453278998, -26.50000000000049738 ) ) ;
#9727=CARTESIAN_POINT ( 'NONE',  ( 35.59419854219520118, 9.774809681453330512, -17.70000000000050022 ) ) ;
#9737=ORIENTED_EDGE ( 'NONE', *, *, #2603, .F. ) ;
#9744=( BOUNDED_CURVE ( )  B_SPLINE_CURVE ( 2, ( #22319, #6061, #8096 ),
 .UNSPECIFIED., .F., .F. ) 
 B_SPLINE_CURVE_WITH_KNOTS ( ( 3, 3 ),
 ( 0.000000000000000000, 0.1752654207116860208 ),
 .UNSPECIFIED. ) 
 CURVE ( )  GEOMETRIC_REPRESENTATION_ITEM ( )  RATIONAL_B_SPLINE_CURVE ( ( 1.000000000000000000, 1.154700538379249908, 1.000000000000000000 ) ) 
 REPRESENTATION_ITEM ( '' )  );
#9878=FACE_OUTER_BOUND ( 'NONE', #14460, .T. ) ;
#9901=VERTEX_POINT ( 'NONE', #10835 ) ;
#9906=ORIENTED_EDGE ( 'NONE', *, *, #5950, .T. ) ;
#9973=ORIENTED_EDGE ( 'NONE', *, *, #17047, .T. ) ;
#10001=ORIENTED_EDGE ( 'NONE', *, *, #7777, .F. ) ;
#10228=EDGE_LOOP ( 'NONE', ( #19844, #13112, #3927, #9130, #21606 ) ) ;
#10267=AXIS2_PLACEMENT_3D ( 'NONE', #8859, #9072, #10884 ) ;
#10277=EDGE_CURVE ( 'NONE', #10416, #965, #3775, .T. ) ;
#10324=DIRECTION ( 'NONE',  ( -6.281952996264290168E-17, -4.969341027148640384E-15, -1.000000000000000000 ) ) ;
#10343=CARTESIAN_POINT ( 'NONE',  ( 38.02679880290970971, 9.198219730472773747, -26.30000000000049809 ) ) ;
#10416=VERTEX_POINT ( 'NONE', #17538 ) ;
#10426=FACE_OUTER_BOUND ( 'NONE', #13425, .T. ) ;
#10481=ORIENTED_EDGE ( 'NONE', *, *, #17047, .F. ) ;
#10486=CARTESIAN_POINT ( 'NONE',  ( 34.49867763533223552, 5.152869186095711207, -27.87500000000047606 ) ) ;
#10526=CARTESIAN_POINT ( 'NONE',  ( 35.09747506357100377, 11.43410645592840069, -29.25000000000050093 ) ) ;
#10628=CARTESIAN_POINT ( 'NONE',  ( 33.90884364377009774, 10.17428291754599989, -29.25000000000050093 ) ) ;
#10680=ORIENTED_EDGE ( 'NONE', *, *, #2327, .F. ) ;
#10763=FACE_OUTER_BOUND ( 'NONE', #11574, .T. ) ;
#10767=TOROIDAL_SURFACE ( 'NONE', #20215, 2.380000000000000338, 2.370000000000000107 ) ;
#10813=DIRECTION ( 'NONE',  ( -0.2867834340965239592, 0.9579954394086668268, -4.742590440343770138E-15 ) ) ;
#10818=ORIENTED_EDGE ( 'NONE', *, *, #7777, .T. ) ;
#10834=ORIENTED_EDGE ( 'NONE', *, *, #7055, .F. ) ;
#10835=CARTESIAN_POINT ( 'NONE',  ( 35.94015251278350576, 11.23436983788199761, -27.55602540378494325 ) ) ;
#10884=DIRECTION ( 'NONE',  ( 0.2306359803922025109, 0.9730401042858035643, -5.112869192352692394E-15 ) ) ;
#10925=EDGE_LOOP ( 'NONE', ( #3788, #13340 ) ) ;
#10946=EDGE_CURVE ( 'NONE', #12386, #19462, #8844, .T. ) ;
#10989=LINE ( 'NONE', #9307, #4525 ) ;
#10992=ORIENTED_EDGE ( 'NONE', *, *, #23444, .T. ) ;
#11004=CARTESIAN_POINT ( 'NONE',  ( 35.59419854219520118, 9.774809681453278998, -26.50000000000049738 ) ) ;
#11063=ORIENTED_EDGE ( 'NONE', *, *, #16049, .F. ) ;
#11071=VERTEX_POINT ( 'NONE', #9669 ) ;
#11096=LINE ( 'NONE', #21635, #21682 ) ;
#11181=ORIENTED_EDGE ( 'NONE', *, *, #22028, .F. ) ;
#11200=DIRECTION ( 'NONE',  ( -0.2306359803922028717, -0.9730401042858035643, 4.849856555169150033E-15 ) ) ;
#11229=EDGE_LOOP ( 'NONE', ( #18279, #15788 ) ) ;
#11232=ORIENTED_EDGE ( 'NONE', *, *, #22410, .F. ) ;
#11255=LINE ( 'NONE', #3634, #7595 ) ;
#11268=DIRECTION ( 'NONE',  ( -6.123230174520380038E-17, -4.962644601432250805E-15, -1.000000000000000000 ) ) ;
#11286=EDGE_CURVE ( 'NONE', #12984, #2526, #20913, .T. ) ;
#11298=FACE_OUTER_BOUND ( 'NONE', #12674, .T. ) ;
#11320=AXIS2_PLACEMENT_3D ( 'NONE', #20386, #9468, #4473 ) ;
#11390=FACE_OUTER_BOUND ( 'NONE', #7791, .T. ) ;
#11419=EDGE_LOOP ( 'NONE', ( #19066, #672, #21596, #22581 ) ) ;
#11447=ADVANCED_FACE ( 'NONE', ( #9272 ), #8650, .T. ) ;
#11488=ORIENTED_EDGE ( 'NONE', *, *, #2236, .F. ) ;
#11569=CYLINDRICAL_SURFACE ( 'NONE', #16536, 4.750000000000001776 ) ;
#11574=EDGE_LOOP ( 'NONE', ( #18273, #19993, #19764, #20504 ) ) ;
#11594=LINE ( 'NONE', #18702, #14148 ) ;
#11668=VERTEX_POINT ( 'NONE', #331 ) ;
#11734=DIRECTION ( 'NONE',  ( -0.2306359803922038432, -0.9730401042858032312, 5.139921410301653163E-15 ) ) ;
#11919=CONICAL_SURFACE ( 'NONE', #20600, 0.8660254037844397068, 1.047197551196598297 ) ;
#11995=AXIS2_PLACEMENT_3D ( 'NONE', #14453, #21679, #19921 ) ;
#11998=ADVANCED_FACE ( 'NONE', ( #7678 ), #16823, .T. ) ;
#12033=EDGE_CURVE ( 'NONE', #22020, #965, #12091, .T. ) ;
#12047=DIRECTION ( 'NONE',  ( 6.281952996264339472E-17, 4.969341027148640384E-15, 1.000000000000000000 ) ) ;
#12091=CIRCLE ( 'NONE', #12825, 2.699999999999998845 ) ;
#12241=AXIS2_PLACEMENT_3D ( 'NONE', #3229, #12047, #15711 ) ;
#12310=EDGE_CURVE ( 'NONE', #9901, #3862, #22753, .T. ) ;
#12332=DIRECTION ( 'NONE',  ( 0.2306359803922029827, 0.9730401042858035643, -4.849856555169146878E-15 ) ) ;
#12345=LINE ( 'NONE', #19324, #866 ) ;
#12367=EDGE_LOOP ( 'NONE', ( #10992, #18756, #4720, #1039, #10834 ) ) ;
#12386=VERTEX_POINT ( 'NONE', #1471 ) ;
#12405=CARTESIAN_POINT ( 'NONE',  ( 35.09747506357100377, 11.43410645592840069, -27.69000000000049866 ) ) ;
#12408=ORIENTED_EDGE ( 'NONE', *, *, #15198, .T. ) ;
#12427=TOROIDAL_SURFACE ( 'NONE', #8624, 2.700000000000000178, 0.2000000000000000111 ) ;
#12474=CARTESIAN_POINT ( 'NONE',  ( 34.40556712239440174, 8.514986143070938596, -29.25000000000050093 ) ) ;
#12498=ORIENTED_EDGE ( 'NONE', *, *, #14756, .F. ) ;
#12546=DIRECTION ( 'NONE',  ( -0.2306359803922025109, -0.9730401042858035643, 5.112869192352692394E-15 ) ) ;
#12608=DIRECTION ( 'NONE',  ( -6.193954341422139021E-17, -4.965628413872130537E-15, -1.000000000000000000 ) ) ;
#12612=EDGE_LOOP ( 'NONE', ( #21694, #19163 ) ) ;
#12651=DIRECTION ( 'NONE',  ( 6.123230174520370177E-17, 4.962644601432260272E-15, 1.000000000000000000 ) ) ;
#12674=EDGE_LOOP ( 'NONE', ( #22285, #3276, #2867, #9620, #17028 ) ) ;
#12739=AXIS2_PLACEMENT_3D ( 'NONE', #2569, #13380, #415 ) ;
#12771=AXIS2_PLACEMENT_3D ( 'NONE', #17152, #9568, #524 ) ;
#12824=VERTEX_POINT ( 'NONE', #7167 ) ;
#12825=AXIS2_PLACEMENT_3D ( 'NONE', #9717, #6130, #11734 ) ;
#12857=EDGE_LOOP ( 'NONE', ( #18012, #14834, #4036, #19664, #10001 ) ) ;
#12863=DIRECTION ( 'NONE',  ( -7.008869410147150310E-16, 5.150359455772420684E-15, 1.000000000000000000 ) ) ;
#12915=ORIENTED_EDGE ( 'NONE', *, *, #15919, .T. ) ;
#12965=CARTESIAN_POINT ( 'NONE',  ( 34.49867763533223552, 5.152869186095713872, -26.88000000000047507 ) ) ;
#12984=VERTEX_POINT ( 'NONE', #12965 ) ;
#13112=ORIENTED_EDGE ( 'NONE', *, *, #2425, .T. ) ;
#13132=EDGE_CURVE ( 'NONE', #7550, #2884, #4647, .T. ) ;
#13149=DIRECTION ( 'NONE',  ( 0.000000000000000000, -1.000000000000000000, 4.969341027148640384E-15 ) ) ;
#13239=CARTESIAN_POINT ( 'NONE',  ( 33.90884364377009774, 10.17428291754599989, -27.69000000000049866 ) ) ;
#13278=ORIENTED_EDGE ( 'NONE', *, *, #15198, .F. ) ;
#13316=DIRECTION ( 'NONE',  ( 0.2306359803922025109, 0.9730401042858035643, -5.112869192352692394E-15 ) ) ;
#13340=ORIENTED_EDGE ( 'NONE', *, *, #16207, .F. ) ;
#13380=DIRECTION ( 'NONE',  ( 0.000000000000000000, 0.000000000000000000, 1.000000000000000000 ) ) ;
#13425=EDGE_LOOP ( 'NONE', ( #13278, #15914, #21923, #9042, #18392, #16859 ) ) ;
#13452=LINE ( 'NONE', #15101, #1761 ) ;
#13482=EDGE_CURVE ( 'NONE', #22277, #5211, #7918, .T. ) ;
#13486=DIRECTION ( 'NONE',  ( -6.123230174520380038E-17, -4.962644601432250805E-15, -1.000000000000000000 ) ) ;
#13650=ORIENTED_EDGE ( 'NONE', *, *, #15918, .T. ) ;
#13781=ORIENTED_EDGE ( 'NONE', *, *, #11286, .T. ) ;
#13832=FACE_OUTER_BOUND ( 'NONE', #14643, .T. ) ;
#13902=CARTESIAN_POINT ( 'NONE',  ( 34.85715660638719982, 8.407947612062049103, -27.55602540378494325 ) ) ;
#13935=CIRCLE ( 'NONE', #5218, 2.500000000000000444 ) ;
#13936=AXIS2_PLACEMENT_3D ( 'NONE', #4653, #8456, #8110 ) ;
#13957=EDGE_CURVE ( 'NONE', #14674, #15708, #19647, .T. ) ;
#13972=DIRECTION ( 'NONE',  ( -7.008869410147150310E-16, 5.150359455772420684E-15, 1.000000000000000000 ) ) ;
#13990=EDGE_CURVE ( 'NONE', #12386, #17514, #22328, .T. ) ;
#14074=CARTESIAN_POINT ( 'NONE',  ( 36.68971944905815974, 14.39675017681084945, -26.50000000000052225 ) ) ;
#14119=CARTESIAN_POINT ( 'NONE',  ( 36.90701083165220098, 10.61980902621680123, -29.25000000000050093 ) ) ;
#14148=VECTOR ( 'NONE', #7763, 1000.000000000000114 ) ;
#14168=TOROIDAL_SURFACE ( 'NONE', #3922, 2.700000000000000178, 0.2000000000000000111 ) ;
#14170=( BOUNDED_CURVE ( )  B_SPLINE_CURVE ( 2, ( #12405, #19634, #3360 ),
 .UNSPECIFIED., .F., .F. ) 
 B_SPLINE_CURVE_WITH_KNOTS ( ( 3, 3 ),
 ( 0.000000000000000000, 0.08763271035584145607 ),
 .UNSPECIFIED. ) 
 CURVE ( )  GEOMETRIC_REPRESENTATION_ITEM ( )  RATIONAL_B_SPLINE_CURVE ( ( 1.000000000000000000, 1.077350269189623511, 1.077350269189624843 ) ) 
 REPRESENTATION_ITEM ( '' )  );
#14194=CARTESIAN_POINT ( 'NONE',  ( 35.59419854219520118, 9.774809681453278998, -26.30000000000050164 ) ) ;
#14246=( NAMED_UNIT ( * ) SI_UNIT ( $, .STERADIAN. ) SOLID_ANGLE_UNIT ( ) );
#14281=CARTESIAN_POINT ( 'NONE',  ( 36.09092202081949807, 8.115512906978191054, -29.25000000000050093 ) ) ;
#14286=DIRECTION ( 'NONE',  ( 0.000000000000000000, -5.179188654504130612E-15, -1.000000000000000000 ) ) ;
#14290=CARTESIAN_POINT ( 'NONE',  ( 35.59419854219520118, 9.774809681453278998, -26.88000000000049994 ) ) ;
#14341=CARTESIAN_POINT ( 'NONE',  ( 35.59419854219520118, 9.774809681453278998, -26.30000000000050164 ) ) ;
#14399=DIRECTION ( 'NONE',  ( -0.7273594590164630391, 0.6862566701892800491, -3.364551046996708737E-15 ) ) ;
#14406=CARTESIAN_POINT ( 'NONE',  ( 35.59419854219520118, 9.774809681453358934, -10.74538000000049998 ) ) ;
#14453=CARTESIAN_POINT ( 'NONE',  ( 35.59419854219520118, 9.774809681453278998, -26.30000000000050164 ) ) ;
#14460=EDGE_LOOP ( 'NONE', ( #18913, #13781, #10680, #454, #1458 ) ) ;
#14467=EDGE_CURVE ( 'NONE', #17514, #1281, #22485, .T. ) ;
#14476=PLANE ( 'NONE',  #17559 ) ;
#14484=AXIS2_PLACEMENT_3D ( 'NONE', #4690, #22954, #17280 ) ;
#14511=EDGE_CURVE ( 'NONE', #1934, #19462, #13452, .T. ) ;
#14577=DIRECTION ( 'NONE',  ( -6.123230174520380038E-17, -4.962644601432250805E-15, -1.000000000000000000 ) ) ;
#14608=DIRECTION ( 'NONE',  ( -0.1997366180463773788, -0.8426774492125681526, -0.4999999999999950595 ) ) ;
#14615=PRODUCT_DEFINITION ( 'UNKNOWN', '', #14812, #17770 ) ;
#14632=AXIS2_PLACEMENT_3D ( 'NONE', #11004, #276, #8875 ) ;
#14643=EDGE_LOOP ( 'NONE', ( #2225, #18343, #7150, #6262 ) ) ;
#14647=FACE_OUTER_BOUND ( 'NONE', #22686, .T. ) ;
#14674=VERTEX_POINT ( 'NONE', #5715 ) ;
#14756=EDGE_CURVE ( 'NONE', #2526, #7180, #1785, .T. ) ;
#14812=PRODUCT_DEFINITION_FORMATION_WITH_SPECIFIED_SOURCE ( 'ANY', '', #19329, .NOT_KNOWN. ) ;
#14834=ORIENTED_EDGE ( 'NONE', *, *, #13132, .T. ) ;
#14925=AXIS2_PLACEMENT_3D ( 'NONE', #1835, #2074, #12546 ) ;
#15001=DIRECTION ( 'NONE',  ( -0.2306359803922019835, -0.9730401042858037863, 4.857225732735059075E-15 ) ) ;
#15011=CARTESIAN_POINT ( 'NONE',  ( 34.15720538308221421, 9.344634530308482567, -27.44000000000048445 ) ) ;
#15062=DIRECTION ( 'NONE',  ( 6.123230174520370177E-17, 4.962644601432260272E-15, 1.000000000000000000 ) ) ;
#15101=CARTESIAN_POINT ( 'NONE',  ( 34.28138625273830087, 8.929810336689708805, -29.25000000000050093 ) ) ;
#15102=VERTEX_POINT ( 'NONE', #329 ) ;
#15109=ORIENTED_EDGE ( 'NONE', *, *, #15327, .F. ) ;
#15129=ORIENTED_EDGE ( 'NONE', *, *, #8486, .F. ) ;
#15155=CYLINDRICAL_SURFACE ( 'NONE', #4972, 2.499999999999997780 ) ;
#15166=ORIENTED_EDGE ( 'NONE', *, *, #21393, .T. ) ;
#15198=EDGE_CURVE ( 'NONE', #21456, #11668, #4274, .T. ) ;
#15327=EDGE_CURVE ( 'NONE', #15708, #12824, #22655, .T. ) ;
#15513=CARTESIAN_POINT ( 'NONE',  ( 35.59419854219520118, 9.774809681453278998, -26.88000000000049994 ) ) ;
#15603=EDGE_CURVE ( 'NONE', #21456, #9901, #7562, .T. ) ;
#15617=VECTOR ( 'NONE', #8075, 999.9999999999998863 ) ;
#15690=AXIS2_PLACEMENT_3D ( 'NONE', #2094, #14577, #20033 ) ;
#15703=VERTEX_POINT ( 'NONE', #7690 ) ;
#15708=VERTEX_POINT ( 'NONE', #18390 ) ;
#15711=DIRECTION ( 'NONE',  ( -0.2306359803922041485, -0.9730401042858032312, 4.373252460445728664E-15 ) ) ;
#15740=CARTESIAN_POINT ( 'NONE',  ( 35.09747506357100377, 11.43410645592840069, -29.25000000000050093 ) ) ;
#15788=ORIENTED_EDGE ( 'NONE', *, *, #13957, .F. ) ;
#15798=ADVANCED_FACE ( 'NONE', ( #13832 ), #21417, .F. ) ;
#15852=FACE_OUTER_BOUND ( 'NONE', #22569, .T. ) ;
#15892=ADVANCED_FACE ( 'NONE', ( #22713 ), #6458, .F. ) ;
#15914=ORIENTED_EDGE ( 'NONE', *, *, #15603, .T. ) ;
#15918=EDGE_CURVE ( 'NONE', #15708, #14674, #2357, .T. ) ;
#15919=EDGE_CURVE ( 'NONE', #14674, #15703, #11096, .T. ) ;
#15928=ORIENTED_EDGE ( 'NONE', *, *, #5299, .F. ) ;
#16032=AXIS2_PLACEMENT_3D ( 'NONE', #21935, #16710, #4134 ) ;
#16049=EDGE_CURVE ( 'NONE', #1281, #9901, #14170, .T. ) ;
#16064=ADVANCED_FACE ( 'NONE', ( #1572 ), #16077, .F. ) ;
#16075=AXIS2_PLACEMENT_3D ( 'NONE', #14341, #11268, #16462 ) ;
#16077=PLANE ( 'NONE',  #18288 ) ;
#16096=CARTESIAN_POINT ( 'NONE',  ( 36.78282996199610722, 11.03463321983559986, -27.69000000000049866 ) ) ;
#16108=( BOUNDED_CURVE ( )  B_SPLINE_CURVE ( 2, ( #23030, #13902, #17943 ),
 .UNSPECIFIED., .F., .F. ) 
 B_SPLINE_CURVE_WITH_KNOTS ( ( 3, 3 ),
 ( 0.08763271035584535573, 0.1752654207116860208 ),
 .UNSPECIFIED. ) 
 CURVE ( )  GEOMETRIC_REPRESENTATION_ITEM ( )  RATIONAL_B_SPLINE_CURVE ( ( 1.077350269189624843, 1.077350269189622844, 1.000000000000000000 ) ) 
 REPRESENTATION_ITEM ( '' )  );
#16137=FACE_OUTER_BOUND ( 'NONE', #11419, .T. ) ;
#16141=( NAMED_UNIT ( * ) PLANE_ANGLE_UNIT ( ) SI_UNIT ( $, .RADIAN. ) );
#16151=CIRCLE ( 'NONE', #14632, 4.750000000000001776 ) ;
#16198=FACE_OUTER_BOUND ( 'NONE', #12367, .T. ) ;
#16206=CARTESIAN_POINT ( 'NONE',  ( 36.33124047800322387, 11.14167175084450889, -27.55602540378493970 ) ) ;
#16207=EDGE_CURVE ( 'NONE', #965, #22020, #5410, .T. ) ;
#16347=FACE_OUTER_BOUND ( 'NONE', #5848, .T. ) ;
#16370=CARTESIAN_POINT ( 'NONE',  ( 35.51881378817719792, 11.33423814690520004, -29.25000000000050093 ) ) ;
#16412=CARTESIAN_POINT ( 'NONE',  ( 36.68523773071988359, 8.745424676169351486, -27.44000000000048445 ) ) ;
#16462=DIRECTION ( 'NONE',  ( -0.2306359803922019835, -0.9730401042858037863, 4.163336342344336238E-15 ) ) ;
#16485=VECTOR ( 'NONE', #18984, 1000.000000000000000 ) ;
#16486=DIRECTION ( 'NONE',  ( -0.9730401042858032312, 0.2306359803922040375, -1.084982917713590005E-15 ) ) ;
#16523=DIRECTION ( 'NONE',  ( -6.281952996264290168E-17, -4.969341027148640384E-15, -1.000000000000000000 ) ) ;
#16532=DIRECTION ( 'NONE',  ( 0.9730401042858034533, -0.2306359803922026774, 1.869849304631839730E-15 ) ) ;
#16533=CARTESIAN_POINT ( 'NONE',  ( 34.20600149872029760, 10.48923880214159965, -29.25000000000050093 ) ) ;
#16536=AXIS2_PLACEMENT_3D ( 'NONE', #16989, #18673, #13316 ) ;
#16616=FACE_OUTER_BOUND ( 'NONE', #2240, .T. ) ;
#16658=EDGE_CURVE ( 'NONE', #5211, #3143, #17583, .T. ) ;
#16661=CARTESIAN_POINT ( 'NONE',  ( 34.49867763533223552, 5.152869186095713872, -26.50000000000047606 ) ) ;
#16686=EDGE_LOOP ( 'NONE', ( #9246, #3223, #10481, #22344 ) ) ;
#16710=DIRECTION ( 'NONE',  ( -0.2306359803922028717, -0.9730401042858035643, 4.849856555169146878E-15 ) ) ;
#16723=AXIS2_PLACEMENT_3D ( 'NONE', #506, #9679, #7760 ) ;
#16739=DIRECTION ( 'NONE',  ( 0.2306359803922020946, 0.9730401042858036753, -4.006172263299086280E-15 ) ) ;
#16743=EDGE_CURVE ( 'NONE', #12984, #21097, #1249, .T. ) ;
#16775=FACE_OUTER_BOUND ( 'NONE', #12857, .T. ) ;
#16789=CARTESIAN_POINT ( 'NONE',  ( 36.09092202081949807, 8.115512906978191054, -27.69000000000049866 ) ) ;
#16823=PLANE ( 'NONE',  #23056 ) ;
#16848=CYLINDRICAL_SURFACE ( 'NONE', #22555, 2.499999999999997780 ) ;
#16859=ORIENTED_EDGE ( 'NONE', *, *, #9691, .T. ) ;
#16863=VERTEX_POINT ( 'NONE', #10343 ) ;
#16884=DIRECTION ( 'NONE',  ( -0.2306359803922038432, -0.9730401042858032312, 5.139921410301653163E-15 ) ) ;
#16901=AXIS2_PLACEMENT_3D ( 'NONE', #7544, #21658, #9086 ) ;
#16989=CARTESIAN_POINT ( 'NONE',  ( 35.59419854219520118, 9.774809681453278998, -27.87500000000050093 ) ) ;
#17028=ORIENTED_EDGE ( 'NONE', *, *, #7027, .F. ) ;
#17047=EDGE_CURVE ( 'NONE', #15102, #2850, #3551, .T. ) ;
#17108=EDGE_CURVE ( 'NONE', #11071, #3143, #21367, .T. ) ;
#17152=CARTESIAN_POINT ( 'NONE',  ( 33.27836309399498305, 10.32372331478672223, -26.88000000000050349 ) ) ;
#17154=CONICAL_SURFACE ( 'NONE', #6992, 0.8660254037844397068, 1.047197551196598297 ) ;
#17161=DIRECTION ( 'NONE',  ( -0.2306359803922019835, -0.9730401042858037863, 4.163336342344336238E-15 ) ) ;
#17280=DIRECTION ( 'NONE',  ( 0.000000000000000000, -4.902758972191440018E-15, -1.000000000000000000 ) ) ;
#17284=CIRCLE ( 'NONE', #11995, 2.500000000000000444 ) ;
#17403=DIRECTION ( 'NONE',  ( -0.2306359803922025109, -0.9730401042858035643, 5.112869192352692394E-15 ) ) ;
#17488=DIRECTION ( 'NONE',  ( 0.9730401042858035643, -0.2306359803922031215, 1.084982917713590597E-15 ) ) ;
#17514=VERTEX_POINT ( 'NONE', #8925 ) ;
#17524=CARTESIAN_POINT ( 'NONE',  ( 32.96699026062352544, 10.39752682851222865, -26.50000000000050093 ) ) ;
#17538=CARTESIAN_POINT ( 'NONE',  ( 33.16159828148068556, 10.35139963243378602, -26.30000000000050520 ) ) ;
#17540=FACE_OUTER_BOUND ( 'NONE', #23000, .T. ) ;
#17541=AXIS2_PLACEMENT_3D ( 'NONE', #9670, #718, #16884 ) ;
#17559=AXIS2_PLACEMENT_3D ( 'NONE', #12474, #9258, #23368 ) ;
#17579=DIRECTION ( 'NONE',  ( -0.2306359803922025109, -0.9730401042858035643, 5.112869192352692394E-15 ) ) ;
#17583=CIRCLE ( 'NONE', #5049, 2.370000000000002771 ) ;
#17606=DIRECTION ( 'NONE',  ( 6.123230174520409620E-17, 4.962644601432260272E-15, 1.000000000000000000 ) ) ;
#17744=CARTESIAN_POINT ( 'NONE',  ( 33.90884364377009774, 10.17428291754599989, -27.69000000000049866 ) ) ;
#17762=DIRECTION ( 'NONE',  ( -6.123230174520380038E-17, -4.962644601432260272E-15, -1.000000000000000000 ) ) ;
#17770=DESIGN_CONTEXT ( 'detailed design', #23228, 'design' ) ;
#17815=VECTOR ( 'NONE', #3488, 1000.000000000000114 ) ;
#17943=CARTESIAN_POINT ( 'NONE',  ( 34.40556712239440174, 8.514986143070949254, -27.69000000000049866 ) ) ;
#17988=DIRECTION ( 'NONE',  ( -6.281952996264309889E-17, -4.969341027148640384E-15, -1.000000000000000000 ) ) ;
#18012=ORIENTED_EDGE ( 'NONE', *, *, #9691, .F. ) ;
#18057=ORIENTED_EDGE ( 'NONE', *, *, #5555, .F. ) ;
#18145=FACE_BOUND ( 'NONE', #19479, .T. ) ;
#18205=FACE_OUTER_BOUND ( 'NONE', #12612, .T. ) ;
#18219=CARTESIAN_POINT ( 'NONE',  ( 35.59419854219520118, 9.774809681453358934, -10.99076000000050080 ) ) ;
#18273=ORIENTED_EDGE ( 'NONE', *, *, #15919, .F. ) ;
#18279=ORIENTED_EDGE ( 'NONE', *, *, #15918, .F. ) ;
#18288=AXIS2_PLACEMENT_3D ( 'NONE', #23305, #7063, #14286 ) ;
#18343=ORIENTED_EDGE ( 'NONE', *, *, #20132, .T. ) ;
#18351=DIRECTION ( 'NONE',  ( 6.123230174520380038E-17, 4.962644601432250805E-15, 1.000000000000000000 ) ) ;
#18390=CARTESIAN_POINT ( 'NONE',  ( 35.13079550495196912, 7.819738582318153775, -10.50000000000049027 ) ) ;
#18392=ORIENTED_EDGE ( 'NONE', *, *, #2852, .T. ) ;
#18393=APPLICATION_CONTEXT ( 'configuration controlled 3d designs of mechanical parts and assemblies' ) ;
#18447=CARTESIAN_POINT ( 'NONE',  ( 36.09092202081949807, 8.115512906978191054, -27.69000000000049866 ) ) ;
#18577=ORIENTED_EDGE ( 'NONE', *, *, #22028, .T. ) ;
#18653=ORIENTED_EDGE ( 'NONE', *, *, #17108, .T. ) ;
#18673=DIRECTION ( 'NONE',  ( 6.123230174520409620E-17, 4.962644601432260272E-15, 1.000000000000000000 ) ) ;
#18683=CARTESIAN_POINT ( 'NONE',  ( 35.24824457160689661, 8.315249525024576371, -27.55602540378494325 ) ) ;
#18702=CARTESIAN_POINT ( 'NONE',  ( 36.98239558567010477, 9.060380560764929925, -29.25000000000050093 ) ) ;
#18756=ORIENTED_EDGE ( 'NONE', *, *, #5555, .T. ) ;
#18780=CARTESIAN_POINT ( 'NONE',  ( 35.39446192414882120, 8.932132232240713066, -27.19000000000049511 ) ) ;
#18872=ORIENTED_EDGE ( 'NONE', *, *, #2425, .F. ) ;
#18913=ORIENTED_EDGE ( 'NONE', *, *, #16743, .F. ) ;
#18984=DIRECTION ( 'NONE',  ( 6.123230174520370177E-17, 4.962644601432260272E-15, 1.000000000000000000 ) ) ;
#19066=ORIENTED_EDGE ( 'NONE', *, *, #13990, .F. ) ;
#19083=CIRCLE ( 'NONE', #19834, 2.500000000000000444 ) ;
#19148=ADVANCED_FACE ( 'NONE', ( #10763 ), #20978, .T. ) ;
#19163=ORIENTED_EDGE ( 'NONE', *, *, #14756, .T. ) ;
#19208=ORIENTED_EDGE ( 'NONE', *, *, #20881, .T. ) ;
#19271=DIRECTION ( 'NONE',  ( -3.715058581704769953E-16, 5.072287515438380936E-15, 1.000000000000000000 ) ) ;
#19282=ADVANCED_FACE ( 'NONE', ( #14647 ), #10767, .T. ) ;
#19324=CARTESIAN_POINT ( 'NONE',  ( 37.27955344062029752, 9.375336445360519022, -28.47000000000049980 ) ) ;
#19329=PRODUCT ( 'Pin 3', 'Pin 3', '', ( #20455 ) ) ;
#19433=DIRECTION ( 'NONE',  ( 0.9730401042858034533, -0.2306359803922026774, 1.869849304631839730E-15 ) ) ;
#19462=VERTEX_POINT ( 'NONE', #2527 ) ;
#19479=EDGE_LOOP ( 'NONE', ( #23379, #9906, #5916, #71, #19208, #9973 ) ) ;
#19487=VECTOR ( 'NONE', #19924, 1000.000000000000000 ) ;
#19529=CARTESIAN_POINT ( 'NONE',  ( 35.59419854219520118, 9.774809681453278998, -26.88000000000049994 ) ) ;
#19566=ADVANCED_FACE ( 'NONE', ( #23159 ), #14168, .F. ) ;
#19632=CARTESIAN_POINT ( 'NONE',  ( 37.27955344062029752, 9.375336445360519022, -27.69000000000049866 ) ) ;
#19634=CARTESIAN_POINT ( 'NONE',  ( 35.54906454756380185, 11.32706792491948278, -27.55602540378494325 ) ) ;
#19647=CIRCLE ( 'NONE', #3333, 2.009239999999998805 ) ;
#19664=ORIENTED_EDGE ( 'NONE', *, *, #10946, .F. ) ;
#19687=AXIS2_PLACEMENT_3D ( 'NONE', #20719, #13486, #17161 ) ;
#19764=ORIENTED_EDGE ( 'NONE', *, *, #15327, .T. ) ;
#19834=AXIS2_PLACEMENT_3D ( 'NONE', #23262, #91, #1645 ) ;
#19844=ORIENTED_EDGE ( 'NONE', *, *, #10277, .F. ) ;
#19848=DIRECTION ( 'NONE',  ( -0.2306359803922040930, -0.9730401042858032312, 4.616450158279817280E-15 ) ) ;
#19921=DIRECTION ( 'NONE',  ( -0.2306359803922019835, -0.9730401042858037863, 4.163336342344336238E-15 ) ) ;
#19924=DIRECTION ( 'NONE',  ( 6.281952996264290168E-17, 4.969341027148640384E-15, 1.000000000000000000 ) ) ;
#19993=ORIENTED_EDGE ( 'NONE', *, *, #13957, .T. ) ;
#20033=DIRECTION ( 'NONE',  ( -0.2306359803922025109, -0.9730401042858035643, 5.112869192352692394E-15 ) ) ;
#20132=EDGE_CURVE ( 'NONE', #3011, #15102, #12345, .T. ) ;
#20147=LINE ( 'NONE', #3871, #7851 ) ;
#20215=AXIS2_PLACEMENT_3D ( 'NONE', #14290, #12863, #16532 ) ;
#20246=CIRCLE ( 'NONE', #12241, 2.380000000000002114 ) ;
#20386=CARTESIAN_POINT ( 'NONE',  ( 35.59419854219520118, 9.774809681453270116, -29.25000000000050093 ) ) ;
#20455=MECHANICAL_CONTEXT ( 'NONE', #18393, 'mechanical' ) ;
#20499=CARTESIAN_POINT ( 'NONE',  ( 36.34169561367309598, 12.92845737834459996, -29.25000000000050093 ) ) ;
#20504=ORIENTED_EDGE ( 'NONE', *, *, #7027, .T. ) ;
#20552=CARTESIAN_POINT ( 'NONE',  ( 35.59419854219520118, 9.774809681453278998, -26.69000000000049866 ) ) ;
#20554=CARTESIAN_POINT ( 'NONE',  ( 33.90884364377009774, 10.17428291754599989, -29.25000000000050093 ) ) ;
#20576=SHAPE_DEFINITION_REPRESENTATION ( #1493, #8415 ) ;
#20600=AXIS2_PLACEMENT_3D ( 'NONE', #8385, #17762, #6617 ) ;
#20601=DIRECTION ( 'NONE',  ( -6.281952996264309889E-17, -4.969341027148640384E-15, -1.000000000000000000 ) ) ;
#20633=ORIENTED_EDGE ( 'NONE', *, *, #22410, .T. ) ;
#20670=LINE ( 'NONE', #2257, #5549 ) ;
#20680=CARTESIAN_POINT ( 'NONE',  ( 35.63933253682661473, 8.222551437987098311, -27.55602540378493970 ) ) ;
#20719=CARTESIAN_POINT ( 'NONE',  ( 35.59419854219520118, 9.774809681453278998, -26.30000000000050164 ) ) ;
#20743=AXIS2_PLACEMENT_3D ( 'NONE', #15513, #13972, #19433 ) ;
#20782=VERTEX_POINT ( 'NONE', #7181 ) ;
#20836=EDGE_LOOP ( 'NONE', ( #22931, #15129, #23089, #15166, #12498 ) ) ;
#20881=EDGE_CURVE ( 'NONE', #2884, #15102, #11594, .T. ) ;
#20913=LINE ( 'NONE', #10486, #1421 ) ;
#20969=CIRCLE ( 'NONE', #16032, 0.2000000000000012046 ) ;
#20978=CONICAL_SURFACE ( 'NONE', #8091, 2.254620000000000068, 0.7853981633974461696 ) ;
#21028=EDGE_CURVE ( 'NONE', #19462, #2884, #22942, .T. ) ;
#21097=VERTEX_POINT ( 'NONE', #23164 ) ;
#21138=DIRECTION ( 'NONE',  ( -6.281952996264290168E-17, -4.969341027148640384E-15, -1.000000000000000000 ) ) ;
#21227=CARTESIAN_POINT ( 'NONE',  ( 40.21613903755276453, 8.679288774590315114, -26.88000000000049283 ) ) ;
#21270=CARTESIAN_POINT ( 'NONE',  ( 35.59419854219520118, 9.774809681453278998, -26.30000000000050164 ) ) ;
#21367=CIRCLE ( 'NONE', #14925, 4.750000000000001776 ) ;
#21393=EDGE_CURVE ( 'NONE', #11071, #7180, #20670, .T. ) ;
#21417=PLANE ( 'NONE',  #14484 ) ;
#21431=DIRECTION ( 'NONE',  ( -3.715058581704769953E-16, 5.072287515438380936E-15, 1.000000000000000000 ) ) ;
#21456=VERTEX_POINT ( 'NONE', #20552 ) ;
#21523=DIRECTION ( 'NONE',  ( 3.121716675495546285E-31, 4.969341027148640384E-15, 1.000000000000000000 ) ) ;
#21596=ORIENTED_EDGE ( 'NONE', *, *, #14511, .F. ) ;
#21606=ORIENTED_EDGE ( 'NONE', *, *, #12033, .T. ) ;
#21635=CARTESIAN_POINT ( 'NONE',  ( 36.11419503630707339, 11.96864536137821666, -10.74538000000051063 ) ) ;
#21645=AXIS2_PLACEMENT_3D ( 'NONE', #3167, #12332, #1476 ) ;
#21658=DIRECTION ( 'NONE',  ( -6.123230174520380038E-17, -4.962644601432250805E-15, -1.000000000000000000 ) ) ;
#21679=DIRECTION ( 'NONE',  ( -6.123230174520380038E-17, -4.962644601432250805E-15, -1.000000000000000000 ) ) ;
#21682=VECTOR ( 'NONE', #5377, 999.9999999999998863 ) ;
#21694=ORIENTED_EDGE ( 'NONE', *, *, #2327, .T. ) ;
#21729=ORIENTED_EDGE ( 'NONE', *, *, #8486, .T. ) ;
#21761=CARTESIAN_POINT ( 'NONE',  ( 36.78282996199610722, 11.03463321983559986, -29.25000000000050093 ) ) ;
#21855=ADVANCED_FACE ( 'NONE', ( #17540 ), #21869, .T. ) ;
#21869=TOROIDAL_SURFACE ( 'NONE', #20743, 2.380000000000000338, 2.370000000000000107 ) ;
#21901=AXIS2_PLACEMENT_3D ( 'NONE', #5574, #12608, #19848 ) ;
#21923=ORIENTED_EDGE ( 'NONE', *, *, #12310, .T. ) ;
#21935=CARTESIAN_POINT ( 'NONE',  ( 38.22140682376687693, 9.152092534394331125, -26.30000000000049809 ) ) ;
#22020=VERTEX_POINT ( 'NONE', #2457 ) ;
#22028=EDGE_CURVE ( 'NONE', #1281, #22077, #20147, .T. ) ;
#22067=AXIS2_PLACEMENT_3D ( 'NONE', #1695, #21523, #5259 ) ;
#22077=VERTEX_POINT ( 'NONE', #15740 ) ;
#22174=ORIENTED_EDGE ( 'NONE', *, *, #13482, .F. ) ;
#22277=VERTEX_POINT ( 'NONE', #3496 ) ;
#22285=ORIENTED_EDGE ( 'NONE', *, *, #5923, .F. ) ;
#22299=DIRECTION ( 'NONE',  ( 0.2306359803922022056, 0.9730401042858037863, -4.163336342344340971E-15 ) ) ;
#22319=CARTESIAN_POINT ( 'NONE',  ( 36.78282996199610722, 11.03463321983559986, -27.69000000000049866 ) ) ;
#22328=( BOUNDED_CURVE ( )  B_SPLINE_CURVE ( 2, ( #7892, #15011, #13239 ),
 .UNSPECIFIED., .F., .F. ) 
 B_SPLINE_CURVE_WITH_KNOTS ( ( 3, 3 ),
 ( 0.000000000000000000, 0.1752654207116860208 ),
 .UNSPECIFIED. ) 
 CURVE ( )  GEOMETRIC_REPRESENTATION_ITEM ( )  RATIONAL_B_SPLINE_CURVE ( ( 1.000000000000000000, 1.154700538379239916, 1.000000000000000000 ) ) 
 REPRESENTATION_ITEM ( '' )  );
#22344=ORIENTED_EDGE ( 'NONE', *, *, #20132, .F. ) ;
#22375=ORIENTED_EDGE ( 'NONE', *, *, #14467, .T. ) ;
#22386=PLANE ( 'NONE',  #128 ) ;
#22410=EDGE_CURVE ( 'NONE', #15703, #12824, #13935, .T. ) ;
#22419=VECTOR ( 'NONE', #14608, 1000.000000000000114 ) ;
#22485=( BOUNDED_CURVE ( )  B_SPLINE_CURVE ( 2, ( #17744, #1450, #8713 ),
 .UNSPECIFIED., .F., .F. ) 
 B_SPLINE_CURVE_WITH_KNOTS ( ( 3, 3 ),
 ( 0.000000000000000000, 0.1752654207116860208 ),
 .UNSPECIFIED. ) 
 CURVE ( )  GEOMETRIC_REPRESENTATION_ITEM ( )  RATIONAL_B_SPLINE_CURVE ( ( 1.000000000000000000, 1.154700538379249908, 1.000000000000000000 ) ) 
 REPRESENTATION_ITEM ( '' )  );
#22555=AXIS2_PLACEMENT_3D ( 'NONE', #4381, #15062, #22299 ) ;
#22557=CARTESIAN_POINT ( 'NONE',  ( 35.59419854219520118, 9.774809681453278998, -27.19000000000049866 ) ) ;
#22569=EDGE_LOOP ( 'NONE', ( #11063, #18577, #11488, #15928, #8902 ) ) ;
#22581=ORIENTED_EDGE ( 'NONE', *, *, #8544, .T. ) ;
#22605=EDGE_LOOP ( 'NONE', ( #2061, #3899, #1372, #11181 ) ) ;
#22655=LINE ( 'NONE', #1036, #15617 ) ;
#22686=EDGE_LOOP ( 'NONE', ( #4636, #8116, #4948, #18653, #8881 ) ) ;
#22713=FACE_OUTER_BOUND ( 'NONE', #22605, .T. ) ;
#22753=( BOUNDED_CURVE ( )  B_SPLINE_CURVE ( 2, ( #1826, #16206, #16096 ),
 .UNSPECIFIED., .F., .F. ) 
 B_SPLINE_CURVE_WITH_KNOTS ( ( 3, 3 ),
 ( 0.08763271035584145607, 0.1752654207116860208 ),
 .UNSPECIFIED. ) 
 CURVE ( )  GEOMETRIC_REPRESENTATION_ITEM ( )  RATIONAL_B_SPLINE_CURVE ( ( 1.077350269189624843, 1.077350269189626175, 1.000000000000000000 ) ) 
 REPRESENTATION_ITEM ( '' )  );
#22931=ORIENTED_EDGE ( 'NONE', *, *, #11286, .F. ) ;
#22942=LINE ( 'NONE', #23054, #4681 ) ;
#22945=ADVANCED_BREP_SHAPE_REPRESENTATION ( '', ( #9573, #12739 ), #3033 ) ;
#22954=DIRECTION ( 'NONE',  ( 0.7273594590164640383, -0.6862566701892790499, 3.364551046996709526E-15 ) ) ;
#23000=EDGE_LOOP ( 'NONE', ( #9737, #4693, #5227, #21729, #8533 ) ) ;
#23012=CARTESIAN_POINT ( 'NONE',  ( 35.59419854219520118, 9.774809681453278998, -26.88000000000049994 ) ) ;
#23030=CARTESIAN_POINT ( 'NONE',  ( 35.24824457160689661, 8.315249525024576371, -27.55602540378494325 ) ) ;
#23054=CARTESIAN_POINT ( 'NONE',  ( 35.66958329621319734, 8.215381216001370390, -29.25000000000050093 ) ) ;
#23056=AXIS2_PLACEMENT_3D ( 'NONE', #2332, #8036, #4230 ) ;
#23089=ORIENTED_EDGE ( 'NONE', *, *, #17108, .F. ) ;
#23104=ADVANCED_FACE ( 'NONE', ( #11298 ), #16848, .T. ) ;
#23159=FACE_OUTER_BOUND ( 'NONE', #10228, .T. ) ;
#23164=CARTESIAN_POINT ( 'NONE',  ( 30.97225804683763073, 10.87033058831624466, -26.88000000000050349 ) ) ;
#23228=APPLICATION_CONTEXT ( 'configuration controlled 3d designs of mechanical parts and assemblies' ) ;
#23262=CARTESIAN_POINT ( 'NONE',  ( 35.59419854219520118, 9.774809681453358934, -10.99076000000050080 ) ) ;
#23276=EDGE_CURVE ( 'NONE', #1644, #15703, #5092, .T. ) ;
#23305=CARTESIAN_POINT ( 'NONE',  ( 36.78282996199610722, 11.03463321983559986, -29.25000000000050093 ) ) ;
#23350=CARTESIAN_POINT ( 'NONE',  ( 33.90884364377009774, 10.17428291754599989, -28.47000000000049980 ) ) ;
#23368=DIRECTION ( 'NONE',  ( -0.2867834340965239592, 0.9579954394086668268, -6.596081495102488335E-32 ) ) ;
#23379=ORIENTED_EDGE ( 'NONE', *, *, #2236, .T. ) ;
#23444=EDGE_CURVE ( 'NONE', #16863, #20782, #17284, .T. ) ;
#23529=COLOUR_RGB('Sky Blue', 0.31764706, 0.68627451, 0.89019608);
#23530=FILL_AREA_STYLE_COLOUR('',#23529);
#23531=FILL_AREA_STYLE('',(#23530));
#23532=SURFACE_STYLE_FILL_AREA(#23531);
#23533=SURFACE_SIDE_STYLE('',(#23532));
#23534=SURFACE_STYLE_USAGE(.BOTH.,#23533);
#23535=PRESENTATION_STYLE_ASSIGNMENT((#23534));
#23629=STYLED_ITEM('',(#23535),#9573);
#23630=MECHANICAL_DESIGN_GEOMETRIC_PRESENTATION_REPRESENTATION('',(#23629),#3033);
ENDSEC;
END-ISO-10303-21;
